ISO-10303-21;
HEADER;
/* Generated by software containing ST-Developer
 * from STEP Tools, Inc. (www.steptools.com) 
 */

FILE_DESCRIPTION(
/* description */ ('Wall-mounted air drop station'),
/* implementation_level */ '2;1');

FILE_NAME(
/* name */ 'M5x70 body screw.step',
/* time_stamp */ '2026-10-28T22:16:19-07:00',
/* author */ (''),
/* organization */ (''),
/* preprocessor_version */ 'ST-DEVELOPER v20.2',
/* originating_system */ 'Autodesk Translation Framework v15.17.0.0',
/* authorisation */ '');

FILE_SCHEMA (('AUTOMOTIVE_DESIGN { 1 0 10303 214 3 1 1 }'));
ENDSEC;

DATA;
#10=MECHANICAL_DESIGN_GEOMETRIC_PRESENTATION_REPRESENTATION('',(#357),#10517);
#251=ORIENTED_CLOSED_SHELL('',*,#5896,.F.);
#254=BREP_WITH_VOIDS('Body1',#5897,(#251));
#267=CONICAL_SURFACE('',#6582,0.4,0.785398163397448);
#268=CONICAL_SURFACE('',#6586,0.41,0.785398163397448);
#269=CONICAL_SURFACE('',#6590,0.26,0.463647609000806);
#299=SHAPE_REPRESENTATION_RELATIONSHIP('SRR','None',#10656,#328);
#328=ADVANCED_BREP_SHAPE_REPRESENTATION('',(#254),#10500);
#357=STYLED_ITEM('',(#10881),#254);
#492=FACE_BOUND('',#1386,.T.);
#493=FACE_BOUND('',#1394,.T.);
#629=PLANE('',#6566);
#630=PLANE('',#6567);
#631=PLANE('',#6568);
#632=PLANE('',#6569);
#633=PLANE('',#6570);
#634=PLANE('',#6571);
#635=PLANE('',#6572);
#636=PLANE('',#6573);
#637=PLANE('',#6574);
#638=PLANE('',#6579);
#639=PLANE('',#6580);
#640=PLANE('',#6588);
#929=FACE_OUTER_BOUND('',#1377,.T.);
#930=FACE_OUTER_BOUND('',#1378,.T.);
#931=FACE_OUTER_BOUND('',#1379,.T.);
#932=FACE_OUTER_BOUND('',#1380,.T.);
#933=FACE_OUTER_BOUND('',#1381,.T.);
#934=FACE_OUTER_BOUND('',#1382,.T.);
#935=FACE_OUTER_BOUND('',#1383,.T.);
#936=FACE_OUTER_BOUND('',#1384,.T.);
#937=FACE_OUTER_BOUND('',#1385,.T.);
#938=FACE_OUTER_BOUND('',#1387,.T.);
#939=FACE_OUTER_BOUND('',#1388,.T.);
#940=FACE_OUTER_BOUND('',#1389,.T.);
#941=FACE_OUTER_BOUND('',#1390,.T.);
#942=FACE_OUTER_BOUND('',#1391,.T.);
#943=FACE_OUTER_BOUND('',#1392,.T.);
#944=FACE_OUTER_BOUND('',#1393,.T.);
#945=FACE_OUTER_BOUND('',#1395,.T.);
#946=FACE_OUTER_BOUND('',#1396,.T.);
#1377=EDGE_LOOP('',(#4711,#4712,#4713,#4714));
#1378=EDGE_LOOP('',(#4715,#4716,#4717,#4718));
#1379=EDGE_LOOP('',(#4719,#4720,#4721,#4722));
#1380=EDGE_LOOP('',(#4723,#4724,#4725,#4726));
#1381=EDGE_LOOP('',(#4727,#4728,#4729,#4730));
#1382=EDGE_LOOP('',(#4731,#4732,#4733,#4734));
#1383=EDGE_LOOP('',(#4735,#4736,#4737,#4738,#4739,#4740));
#1384=EDGE_LOOP('',(#4741,#4742,#4743,#4744,#4745,#4746));
#1385=EDGE_LOOP('',(#4747));
#1386=EDGE_LOOP('',(#4748));
#1387=EDGE_LOOP('',(#4749,#4750,#4751,#4752));
#1388=EDGE_LOOP('',(#4753));
#1389=EDGE_LOOP('',(#4754));
#1390=EDGE_LOOP('',(#4755,#4756,#4757,#4758));
#1391=EDGE_LOOP('',(#4759,#4760,#4761,#4762));
#1392=EDGE_LOOP('',(#4763,#4764,#4765,#4766));
#1393=EDGE_LOOP('',(#4767));
#1394=EDGE_LOOP('',(#4768));
#1395=EDGE_LOOP('',(#4769,#4770,#4771,#4772));
#1396=EDGE_LOOP('',(#4773,#4774,#4775,#4776));
#1820=LINE('',#9574,#2284);
#1821=LINE('',#9576,#2285);
#1822=LINE('',#9578,#2286);
#1823=LINE('',#9579,#2287);
#1824=LINE('',#9582,#2288);
#1825=LINE('',#9584,#2289);
#1826=LINE('',#9585,#2290);
#1827=LINE('',#9588,#2291);
#1828=LINE('',#9590,#2292);
#1829=LINE('',#9591,#2293);
#1830=LINE('',#9594,#2294);
#1831=LINE('',#9596,#2295);
#1832=LINE('',#9597,#2296);
#1833=LINE('',#9600,#2297);
#1834=LINE('',#9602,#2298);
#1835=LINE('',#9603,#2299);
#1836=LINE('',#9605,#2300);
#1837=LINE('',#9606,#2301);
#1838=LINE('',#9616,#2302);
#1839=LINE('',#9625,#2303);
#1840=LINE('',#9629,#2304);
#1841=LINE('',#9633,#2305);
#1842=LINE('',#9640,#2306);
#1843=LINE('',#9642,#2307);
#2284=VECTOR('',#7816,1.);
#2285=VECTOR('',#7817,1.);
#2286=VECTOR('',#7818,1.);
#2287=VECTOR('',#7819,1.);
#2288=VECTOR('',#7822,1.);
#2289=VECTOR('',#7823,1.);
#2290=VECTOR('',#7824,1.);
#2291=VECTOR('',#7827,1.);
#2292=VECTOR('',#7828,1.);
#2293=VECTOR('',#7829,1.);
#2294=VECTOR('',#7832,1.);
#2295=VECTOR('',#7833,1.);
#2296=VECTOR('',#7834,1.);
#2297=VECTOR('',#7837,1.);
#2298=VECTOR('',#7838,1.);
#2299=VECTOR('',#7839,1.);
#2300=VECTOR('',#7842,1.);
#2301=VECTOR('',#7843,1.);
#2302=VECTOR('',#7856,0.25);
#2303=VECTOR('',#7869,0.4);
#2304=VECTOR('',#7874,0.425);
#2305=VECTOR('',#7879,0.41);
#2306=VECTOR('',#7888,0.26);
#2307=VECTOR('',#7891,0.25);
#2661=CIRCLE('',#6575,0.25);
#2662=CIRCLE('',#6576,0.24505);
#2663=CIRCLE('',#6578,0.25);
#2664=CIRCLE('',#6581,0.375);
#2665=CIRCLE('',#6583,0.425);
#2666=CIRCLE('',#6585,0.425);
#2667=CIRCLE('',#6587,0.395);
#2668=CIRCLE('',#6589,0.27);
#2669=CIRCLE('',#6591,0.24505);
#3011=VERTEX_POINT('',#9572);
#3012=VERTEX_POINT('',#9573);
#3013=VERTEX_POINT('',#9575);
#3014=VERTEX_POINT('',#9577);
#3015=VERTEX_POINT('',#9581);
#3016=VERTEX_POINT('',#9583);
#3017=VERTEX_POINT('',#9587);
#3018=VERTEX_POINT('',#9589);
#3019=VERTEX_POINT('',#9593);
#3020=VERTEX_POINT('',#9595);
#3021=VERTEX_POINT('',#9599);
#3022=VERTEX_POINT('',#9601);
#3023=VERTEX_POINT('',#9610);
#3024=VERTEX_POINT('',#9612);
#3025=VERTEX_POINT('',#9615);
#3026=VERTEX_POINT('',#9620);
#3027=VERTEX_POINT('',#9623);
#3028=VERTEX_POINT('',#9627);
#3029=VERTEX_POINT('',#9631);
#3030=VERTEX_POINT('',#9635);
#3031=VERTEX_POINT('',#9638);
#3613=EDGE_CURVE('',#3011,#3012,#1820,.T.);
#3614=EDGE_CURVE('',#3012,#3013,#1821,.T.);
#3615=EDGE_CURVE('',#3013,#3014,#1822,.T.);
#3616=EDGE_CURVE('',#3011,#3014,#1823,.T.);
#3617=EDGE_CURVE('',#3012,#3015,#1824,.T.);
#3618=EDGE_CURVE('',#3015,#3016,#1825,.T.);
#3619=EDGE_CURVE('',#3016,#3013,#1826,.T.);
#3620=EDGE_CURVE('',#3015,#3017,#1827,.T.);
#3621=EDGE_CURVE('',#3017,#3018,#1828,.T.);
#3622=EDGE_CURVE('',#3018,#3016,#1829,.T.);
#3623=EDGE_CURVE('',#3017,#3019,#1830,.T.);
#3624=EDGE_CURVE('',#3019,#3020,#1831,.T.);
#3625=EDGE_CURVE('',#3020,#3018,#1832,.T.);
#3626=EDGE_CURVE('',#3019,#3021,#1833,.T.);
#3627=EDGE_CURVE('',#3021,#3022,#1834,.T.);
#3628=EDGE_CURVE('',#3022,#3020,#1835,.T.);
#3629=EDGE_CURVE('',#3021,#3011,#1836,.T.);
#3630=EDGE_CURVE('',#3014,#3022,#1837,.T.);
#3631=EDGE_CURVE('',#3023,#3023,#2661,.T.);
#3632=EDGE_CURVE('',#3024,#3024,#2662,.T.);
#3633=EDGE_CURVE('',#3023,#3025,#1838,.T.);
#3634=EDGE_CURVE('',#3025,#3025,#2663,.T.);
#3635=EDGE_CURVE('',#3026,#3026,#2664,.T.);
#3636=EDGE_CURVE('',#3027,#3027,#2665,.T.);
#3637=EDGE_CURVE('',#3027,#3026,#1839,.T.);
#3638=EDGE_CURVE('',#3028,#3028,#2666,.T.);
#3639=EDGE_CURVE('',#3028,#3027,#1840,.T.);
#3640=EDGE_CURVE('',#3029,#3029,#2667,.T.);
#3641=EDGE_CURVE('',#3029,#3028,#1841,.T.);
#3642=EDGE_CURVE('',#3030,#3030,#2668,.T.);
#3643=EDGE_CURVE('',#3031,#3031,#2669,.F.);
#3644=EDGE_CURVE('',#3031,#3030,#1842,.T.);
#3645=EDGE_CURVE('',#3024,#3031,#1843,.T.);
#4711=ORIENTED_EDGE('',*,*,#3613,.T.);
#4712=ORIENTED_EDGE('',*,*,#3614,.T.);
#4713=ORIENTED_EDGE('',*,*,#3615,.T.);
#4714=ORIENTED_EDGE('',*,*,#3616,.F.);
#4715=ORIENTED_EDGE('',*,*,#3617,.T.);
#4716=ORIENTED_EDGE('',*,*,#3618,.T.);
#4717=ORIENTED_EDGE('',*,*,#3619,.T.);
#4718=ORIENTED_EDGE('',*,*,#3614,.F.);
#4719=ORIENTED_EDGE('',*,*,#3620,.T.);
#4720=ORIENTED_EDGE('',*,*,#3621,.T.);
#4721=ORIENTED_EDGE('',*,*,#3622,.T.);
#4722=ORIENTED_EDGE('',*,*,#3618,.F.);
#4723=ORIENTED_EDGE('',*,*,#3623,.T.);
#4724=ORIENTED_EDGE('',*,*,#3624,.T.);
#4725=ORIENTED_EDGE('',*,*,#3625,.T.);
#4726=ORIENTED_EDGE('',*,*,#3621,.F.);
#4727=ORIENTED_EDGE('',*,*,#3626,.T.);
#4728=ORIENTED_EDGE('',*,*,#3627,.T.);
#4729=ORIENTED_EDGE('',*,*,#3628,.T.);
#4730=ORIENTED_EDGE('',*,*,#3624,.F.);
#4731=ORIENTED_EDGE('',*,*,#3629,.T.);
#4732=ORIENTED_EDGE('',*,*,#3616,.T.);
#4733=ORIENTED_EDGE('',*,*,#3630,.T.);
#4734=ORIENTED_EDGE('',*,*,#3627,.F.);
#4735=ORIENTED_EDGE('',*,*,#3629,.F.);
#4736=ORIENTED_EDGE('',*,*,#3626,.F.);
#4737=ORIENTED_EDGE('',*,*,#3623,.F.);
#4738=ORIENTED_EDGE('',*,*,#3620,.F.);
#4739=ORIENTED_EDGE('',*,*,#3617,.F.);
#4740=ORIENTED_EDGE('',*,*,#3613,.F.);
#4741=ORIENTED_EDGE('',*,*,#3630,.F.);
#4742=ORIENTED_EDGE('',*,*,#3615,.F.);
#4743=ORIENTED_EDGE('',*,*,#3619,.F.);
#4744=ORIENTED_EDGE('',*,*,#3622,.F.);
#4745=ORIENTED_EDGE('',*,*,#3625,.F.);
#4746=ORIENTED_EDGE('',*,*,#3628,.F.);
#4747=ORIENTED_EDGE('',*,*,#3631,.T.);
#4748=ORIENTED_EDGE('',*,*,#3632,.F.);
#4749=ORIENTED_EDGE('',*,*,#3631,.F.);
#4750=ORIENTED_EDGE('',*,*,#3633,.T.);
#4751=ORIENTED_EDGE('',*,*,#3634,.T.);
#4752=ORIENTED_EDGE('',*,*,#3633,.F.);
#4753=ORIENTED_EDGE('',*,*,#3634,.F.);
#4754=ORIENTED_EDGE('',*,*,#3635,.F.);
#4755=ORIENTED_EDGE('',*,*,#3636,.F.);
#4756=ORIENTED_EDGE('',*,*,#3637,.T.);
#4757=ORIENTED_EDGE('',*,*,#3635,.T.);
#4758=ORIENTED_EDGE('',*,*,#3637,.F.);
#4759=ORIENTED_EDGE('',*,*,#3638,.F.);
#4760=ORIENTED_EDGE('',*,*,#3639,.T.);
#4761=ORIENTED_EDGE('',*,*,#3636,.T.);
#4762=ORIENTED_EDGE('',*,*,#3639,.F.);
#4763=ORIENTED_EDGE('',*,*,#3640,.F.);
#4764=ORIENTED_EDGE('',*,*,#3641,.T.);
#4765=ORIENTED_EDGE('',*,*,#3638,.T.);
#4766=ORIENTED_EDGE('',*,*,#3641,.F.);
#4767=ORIENTED_EDGE('',*,*,#3640,.T.);
#4768=ORIENTED_EDGE('',*,*,#3642,.F.);
#4769=ORIENTED_EDGE('',*,*,#3643,.F.);
#4770=ORIENTED_EDGE('',*,*,#3644,.T.);
#4771=ORIENTED_EDGE('',*,*,#3642,.T.);
#4772=ORIENTED_EDGE('',*,*,#3644,.F.);
#4773=ORIENTED_EDGE('',*,*,#3632,.T.);
#4774=ORIENTED_EDGE('',*,*,#3645,.T.);
#4775=ORIENTED_EDGE('',*,*,#3643,.T.);
#4776=ORIENTED_EDGE('',*,*,#3645,.F.);
#5495=CYLINDRICAL_SURFACE('',#6577,0.25);
#5496=CYLINDRICAL_SURFACE('',#6584,0.425);
#5497=CYLINDRICAL_SURFACE('',#6592,0.24505);
#5702=ADVANCED_FACE('',(#929),#629,.F.);
#5703=ADVANCED_FACE('',(#930),#630,.F.);
#5704=ADVANCED_FACE('',(#931),#631,.F.);
#5705=ADVANCED_FACE('',(#932),#632,.F.);
#5706=ADVANCED_FACE('',(#933),#633,.F.);
#5707=ADVANCED_FACE('',(#934),#634,.F.);
#5708=ADVANCED_FACE('',(#935),#635,.F.);
#5709=ADVANCED_FACE('',(#936),#636,.F.);
#5710=ADVANCED_FACE('',(#937,#492),#637,.T.);
#5711=ADVANCED_FACE('',(#938),#5495,.T.);
#5712=ADVANCED_FACE('',(#939),#638,.F.);
#5713=ADVANCED_FACE('',(#940),#639,.T.);
#5714=ADVANCED_FACE('',(#941),#267,.T.);
#5715=ADVANCED_FACE('',(#942),#5496,.T.);
#5716=ADVANCED_FACE('',(#943),#268,.T.);
#5717=ADVANCED_FACE('',(#944,#493),#640,.T.);
#5718=ADVANCED_FACE('',(#945),#269,.T.);
#5719=ADVANCED_FACE('',(#946),#5497,.T.);
#5896=CLOSED_SHELL('',(#5702,#5703,#5704,#5705,#5706,#5707,#5708,#5709));
#5897=CLOSED_SHELL('',(#5710,#5711,#5712,#5713,#5714,#5715,#5716,#5717,
#5718,#5719));
#6565=AXIS2_PLACEMENT_3D('',#9570,#7812,#7813);
#6566=AXIS2_PLACEMENT_3D('',#9571,#7814,#7815);
#6567=AXIS2_PLACEMENT_3D('',#9580,#7820,#7821);
#6568=AXIS2_PLACEMENT_3D('',#9586,#7825,#7826);
#6569=AXIS2_PLACEMENT_3D('',#9592,#7830,#7831);
#6570=AXIS2_PLACEMENT_3D('',#9598,#7835,#7836);
#6571=AXIS2_PLACEMENT_3D('',#9604,#7840,#7841);
#6572=AXIS2_PLACEMENT_3D('',#9607,#7844,#7845);
#6573=AXIS2_PLACEMENT_3D('',#9608,#7846,#7847);
#6574=AXIS2_PLACEMENT_3D('',#9609,#7848,#7849);
#6575=AXIS2_PLACEMENT_3D('',#9611,#7850,#7851);
#6576=AXIS2_PLACEMENT_3D('',#9613,#7852,#7853);
#6577=AXIS2_PLACEMENT_3D('',#9614,#7854,#7855);
#6578=AXIS2_PLACEMENT_3D('',#9617,#7857,#7858);
#6579=AXIS2_PLACEMENT_3D('',#9618,#7859,#7860);
#6580=AXIS2_PLACEMENT_3D('',#9619,#7861,#7862);
#6581=AXIS2_PLACEMENT_3D('',#9621,#7863,#7864);
#6582=AXIS2_PLACEMENT_3D('',#9622,#7865,#7866);
#6583=AXIS2_PLACEMENT_3D('',#9624,#7867,#7868);
#6584=AXIS2_PLACEMENT_3D('',#9626,#7870,#7871);
#6585=AXIS2_PLACEMENT_3D('',#9628,#7872,#7873);
#6586=AXIS2_PLACEMENT_3D('',#9630,#7875,#7876);
#6587=AXIS2_PLACEMENT_3D('',#9632,#7877,#7878);
#6588=AXIS2_PLACEMENT_3D('',#9634,#7880,#7881);
#6589=AXIS2_PLACEMENT_3D('',#9636,#7882,#7883);
#6590=AXIS2_PLACEMENT_3D('',#9637,#7884,#7885);
#6591=AXIS2_PLACEMENT_3D('',#9639,#7886,#7887);
#6592=AXIS2_PLACEMENT_3D('',#9641,#7889,#7890);
#7812=DIRECTION('axis',(0.,0.,1.));
#7813=DIRECTION('refdir',(1.,0.,0.));
#7814=DIRECTION('center_axis',(0.866025403784439,0.,-0.5));
#7815=DIRECTION('ref_axis',(0.5,0.,0.866025403784439));
#7816=DIRECTION('',(-0.5,0.,-0.866025403784439));
#7817=DIRECTION('',(0.,-1.,0.));
#7818=DIRECTION('',(0.5,0.,0.866025403784439));
#7819=DIRECTION('',(0.,-1.,0.));
#7820=DIRECTION('center_axis',(1.20185167898973E-16,0.,-1.));
#7821=DIRECTION('ref_axis',(1.,0.,1.20185167898973E-16));
#7822=DIRECTION('',(-1.,0.,-1.20185167898973E-16));
#7823=DIRECTION('',(0.,-1.,0.));
#7824=DIRECTION('',(1.,0.,1.20185167898973E-16));
#7825=DIRECTION('center_axis',(-0.866025403784439,0.,-0.5));
#7826=DIRECTION('ref_axis',(0.5,0.,-0.866025403784439));
#7827=DIRECTION('',(-0.5,0.,0.866025403784439));
#7828=DIRECTION('',(0.,-1.,0.));
#7829=DIRECTION('',(0.5,0.,-0.866025403784439));
#7830=DIRECTION('center_axis',(-0.866025403784439,0.,0.5));
#7831=DIRECTION('ref_axis',(-0.5,0.,-0.866025403784439));
#7832=DIRECTION('',(0.5,0.,0.866025403784439));
#7833=DIRECTION('',(0.,-1.,0.));
#7834=DIRECTION('',(-0.5,0.,-0.866025403784439));
#7835=DIRECTION('center_axis',(-2.40370335797945E-16,0.,1.));
#7836=DIRECTION('ref_axis',(-1.,0.,-2.40370335797945E-16));
#7837=DIRECTION('',(1.,0.,2.40370335797945E-16));
#7838=DIRECTION('',(0.,-1.,0.));
#7839=DIRECTION('',(-1.,0.,-2.40370335797945E-16));
#7840=DIRECTION('center_axis',(0.866025403784439,0.,0.5));
#7841=DIRECTION('ref_axis',(-0.5,0.,0.866025403784439));
#7842=DIRECTION('',(0.5,0.,-0.866025403784439));
#7843=DIRECTION('',(-0.5,0.,0.866025403784439));
#7844=DIRECTION('center_axis',(0.,1.,0.));
#7845=DIRECTION('ref_axis',(1.,0.,0.));
#7846=DIRECTION('center_axis',(0.,-1.,0.));
#7847=DIRECTION('ref_axis',(0.,0.,-1.));
#7848=DIRECTION('center_axis',(0.,1.,0.));
#7849=DIRECTION('ref_axis',(1.,0.,0.));
#7850=DIRECTION('center_axis',(0.,1.,0.));
#7851=DIRECTION('ref_axis',(1.,0.,0.));
#7852=DIRECTION('center_axis',(0.,1.,0.));
#7853=DIRECTION('ref_axis',(1.,0.,0.));
#7854=DIRECTION('center_axis',(0.,1.,0.));
#7855=DIRECTION('ref_axis',(1.,0.,0.));
#7856=DIRECTION('',(0.,-1.,0.));
#7857=DIRECTION('center_axis',(0.,1.,0.));
#7858=DIRECTION('ref_axis',(1.,0.,0.));
#7859=DIRECTION('center_axis',(0.,1.,0.));
#7860=DIRECTION('ref_axis',(1.,0.,0.));
#7861=DIRECTION('center_axis',(0.,1.,0.));
#7862=DIRECTION('ref_axis',(0.,0.,1.));
#7863=DIRECTION('center_axis',(0.,-1.,0.));
#7864=DIRECTION('ref_axis',(1.,0.,0.));
#7865=DIRECTION('center_axis',(0.,-1.,0.));
#7866=DIRECTION('ref_axis',(1.,0.,0.));
#7867=DIRECTION('center_axis',(0.,-1.,0.));
#7868=DIRECTION('ref_axis',(1.,0.,0.));
#7869=DIRECTION('',(0.707106781186548,0.707106781186547,8.65956056235493E-17));
#7870=DIRECTION('center_axis',(0.,-1.,0.));
#7871=DIRECTION('ref_axis',(1.,0.,0.));
#7872=DIRECTION('center_axis',(0.,-1.,0.));
#7873=DIRECTION('ref_axis',(1.,0.,0.));
#7874=DIRECTION('',(0.,1.,0.));
#7875=DIRECTION('center_axis',(0.,1.,0.));
#7876=DIRECTION('ref_axis',(1.,0.,0.));
#7877=DIRECTION('center_axis',(0.,-1.,0.));
#7878=DIRECTION('ref_axis',(1.,0.,0.));
#7879=DIRECTION('',(-0.707106781186547,0.707106781186548,-8.65956056235493E-17));
#7880=DIRECTION('center_axis',(0.,-1.,0.));
#7881=DIRECTION('ref_axis',(0.,0.,-1.));
#7882=DIRECTION('center_axis',(0.,-1.,0.));
#7883=DIRECTION('ref_axis',(1.,0.,0.));
#7884=DIRECTION('center_axis',(0.,1.,0.));
#7885=DIRECTION('ref_axis',(1.,0.,0.));
#7886=DIRECTION('center_axis',(0.,1.,0.));
#7887=DIRECTION('ref_axis',(1.,0.,0.));
#7888=DIRECTION('',(-0.447213595499958,0.894427190999916,-5.47678698264203E-17));
#7889=DIRECTION('center_axis',(0.,-1.,0.));
#7890=DIRECTION('ref_axis',(1.,0.,0.));
#7891=DIRECTION('',(0.,1.,0.));
#9570=CARTESIAN_POINT('',(0.,0.,0.));
#9571=CARTESIAN_POINT('Origin',(0.115470053837925,-0.5,-0.2));
#9572=CARTESIAN_POINT('',(0.23094010767585,-0.5,0.));
#9573=CARTESIAN_POINT('',(0.115470053837925,-0.5,-0.2));
#9574=CARTESIAN_POINT('',(0.23094010767585,-0.5,0.));
#9575=CARTESIAN_POINT('',(0.115470053837925,-0.8,-0.2));
#9576=CARTESIAN_POINT('',(0.115470053837925,-0.5,-0.2));
#9577=CARTESIAN_POINT('',(0.23094010767585,-0.8,0.));
#9578=CARTESIAN_POINT('',(0.23094010767585,-0.8,0.));
#9579=CARTESIAN_POINT('',(0.23094010767585,-0.5,0.));
#9580=CARTESIAN_POINT('Origin',(-0.115470053837925,-0.5,-0.2));
#9581=CARTESIAN_POINT('',(-0.115470053837925,-0.5,-0.2));
#9582=CARTESIAN_POINT('',(0.115470053837925,-0.5,-0.2));
#9583=CARTESIAN_POINT('',(-0.115470053837925,-0.8,-0.2));
#9584=CARTESIAN_POINT('',(-0.115470053837925,-0.5,-0.2));
#9585=CARTESIAN_POINT('',(0.115470053837925,-0.8,-0.2));
#9586=CARTESIAN_POINT('Origin',(-0.23094010767585,-0.5,-2.77555756156289E-17));
#9587=CARTESIAN_POINT('',(-0.23094010767585,-0.5,-2.82820063659975E-17));
#9588=CARTESIAN_POINT('',(-0.115470053837925,-0.5,-0.2));
#9589=CARTESIAN_POINT('',(-0.23094010767585,-0.8,-2.77555756156289E-17));
#9590=CARTESIAN_POINT('',(-0.23094010767585,-0.5,-2.82820063659975E-17));
#9591=CARTESIAN_POINT('',(-0.115470053837925,-0.8,-0.2));
#9592=CARTESIAN_POINT('Origin',(-0.115470053837925,-0.5,0.2));
#9593=CARTESIAN_POINT('',(-0.115470053837925,-0.5,0.2));
#9594=CARTESIAN_POINT('',(-0.23094010767585,-0.5,-2.82820063659975E-17));
#9595=CARTESIAN_POINT('',(-0.115470053837925,-0.8,0.2));
#9596=CARTESIAN_POINT('',(-0.115470053837925,-0.5,0.2));
#9597=CARTESIAN_POINT('',(-0.23094010767585,-0.8,-2.82820063659975E-17));
#9598=CARTESIAN_POINT('Origin',(0.115470053837925,-0.5,0.2));
#9599=CARTESIAN_POINT('',(0.115470053837925,-0.5,0.2));
#9600=CARTESIAN_POINT('',(-0.115470053837925,-0.5,0.2));
#9601=CARTESIAN_POINT('',(0.115470053837925,-0.8,0.2));
#9602=CARTESIAN_POINT('',(0.115470053837925,-0.5,0.2));
#9603=CARTESIAN_POINT('',(-0.115470053837925,-0.8,0.2));
#9604=CARTESIAN_POINT('Origin',(0.23094010767585,-0.5,0.));
#9605=CARTESIAN_POINT('',(0.115470053837925,-0.5,0.2));
#9606=CARTESIAN_POINT('',(0.115470053837925,-0.8,0.2));
#9607=CARTESIAN_POINT('Origin',(0.,-0.5,0.));
#9608=CARTESIAN_POINT('Origin',(0.,-0.8,0.));
#9609=CARTESIAN_POINT('Origin',(0.,-1.9,0.));
#9610=CARTESIAN_POINT('',(-0.25,-1.9,3.06161699786838E-17));
#9611=CARTESIAN_POINT('Origin',(0.,-1.9,0.));
#9612=CARTESIAN_POINT('',(-0.24505,-1.9,3.00099698131059E-17));
#9613=CARTESIAN_POINT('Origin',(0.,-1.9,0.));
#9614=CARTESIAN_POINT('Origin',(0.,-7.,0.));
#9615=CARTESIAN_POINT('',(-0.25,-7.,3.06161699786838E-17));
#9616=CARTESIAN_POINT('',(-0.25,-7.,3.06161699786838E-17));
#9617=CARTESIAN_POINT('Origin',(0.,-7.,0.));
#9618=CARTESIAN_POINT('Origin',(0.,-7.,0.));
#9619=CARTESIAN_POINT('Origin',(0.375,0.5,0.));
#9620=CARTESIAN_POINT('',(-0.375,0.5,-4.59242549680257E-17));
#9621=CARTESIAN_POINT('Origin',(0.,0.5,0.));
#9622=CARTESIAN_POINT('Origin',(0.,0.475,0.));
#9623=CARTESIAN_POINT('',(-0.425,0.45,-5.20474889637625E-17));
#9624=CARTESIAN_POINT('Origin',(0.,0.45,0.));
#9625=CARTESIAN_POINT('',(-0.4,0.475,-4.89858719658941E-17));
#9626=CARTESIAN_POINT('Origin',(0.,0.24,0.));
#9627=CARTESIAN_POINT('',(-0.425,0.0299999999999998,-5.20474889637625E-17));
#9628=CARTESIAN_POINT('Origin',(0.,0.0299999999999998,0.));
#9629=CARTESIAN_POINT('',(-0.425,0.24,-5.20474889637625E-17));
#9630=CARTESIAN_POINT('Origin',(0.,0.0150000000000001,0.));
#9631=CARTESIAN_POINT('',(-0.395,4.85722573273506E-17,-4.83735485663204E-17));
#9632=CARTESIAN_POINT('Origin',(0.,0.,0.));
#9633=CARTESIAN_POINT('',(-0.41,0.0150000000000001,-5.02105187650415E-17));
#9634=CARTESIAN_POINT('Origin',(0.27,0.,0.));
#9635=CARTESIAN_POINT('',(-0.27,0.,-3.30654635769785E-17));
#9636=CARTESIAN_POINT('Origin',(0.,0.,0.));
#9637=CARTESIAN_POINT('Origin',(0.,-0.02,0.));
#9638=CARTESIAN_POINT('',(-0.24505,-0.0498999999999999,3.00099698131059E-17));
#9639=CARTESIAN_POINT('Origin',(0.,-0.0498999999999999,0.));
#9640=CARTESIAN_POINT('',(-0.26,-0.02,-3.18408167778312E-17));
#9641=CARTESIAN_POINT('Origin',(0.,-0.995,0.));
#9642=CARTESIAN_POINT('',(-0.24505,-0.995,-3.00099698131059E-17));
#10467=UNCERTAINTY_MEASURE_WITH_UNIT(LENGTH_MEASURE(0.001),#10518,
'DISTANCE_ACCURACY_VALUE',
'Maximum model space distance between geometric entities at asserted c
onnectivities');
#10484=UNCERTAINTY_MEASURE_WITH_UNIT(LENGTH_MEASURE(0.001),#10518,
'DISTANCE_ACCURACY_VALUE',
'Maximum model space distance between geometric entities at asserted c
onnectivities');
#10500=(
GEOMETRIC_REPRESENTATION_CONTEXT(3)
GLOBAL_UNCERTAINTY_ASSIGNED_CONTEXT((#10467))
GLOBAL_UNIT_ASSIGNED_CONTEXT((#10518,#10520,#10521))
REPRESENTATION_CONTEXT('','3D')
);
#10517=(
GEOMETRIC_REPRESENTATION_CONTEXT(3)
GLOBAL_UNCERTAINTY_ASSIGNED_CONTEXT((#10484))
GLOBAL_UNIT_ASSIGNED_CONTEXT((#10518,#10520,#10521))
REPRESENTATION_CONTEXT('','3D')
);
#10518=(
LENGTH_UNIT()
NAMED_UNIT(*)
SI_UNIT(.CENTI.,.METRE.)
);
#10520=(
NAMED_UNIT(*)
PLANE_ANGLE_UNIT()
SI_UNIT($,.RADIAN.)
);
#10521=(
NAMED_UNIT(*)
SI_UNIT($,.STERADIAN.)
SOLID_ANGLE_UNIT()
);
#10537=SHAPE_DEFINITION_REPRESENTATION(#10569,#10656);
#10569=PRODUCT_DEFINITION_SHAPE('',$,#10689);
#10656=SHAPE_REPRESENTATION('',(#6565),#10500);
#10673=PRODUCT_DEFINITION_CONTEXT('part definition',#10771,'design');
#10689=PRODUCT_DEFINITION('M5x70 body screw','M5x70 body screw',#10721,
#10673);
#10721=PRODUCT_DEFINITION_FORMATION('',$,#10788);
#10771=APPLICATION_CONTEXT(
'Core Data for Automotive Mechanical Design Process');
#10772=PRODUCT_CONTEXT('part definition',#10771,'mechanical');
#10788=PRODUCT('M5x70 body screw','M5x70 body screw','M5x70 body screw',
(#10772));
#10875=COLOUR_RGB('Black',0.12,0.14,0.17);
#10876=FILL_AREA_STYLE_COLOUR('',#10875);
#10877=FILL_AREA_STYLE('',(#10876));
#10878=SURFACE_STYLE_FILL_AREA(#10877);
#10879=SURFACE_SIDE_STYLE('',(#10878));
#10880=SURFACE_STYLE_USAGE(.BOTH.,#10879);
#10881=PRESENTATION_STYLE_ASSIGNMENT((#10880));
ENDSEC;
END-ISO-10303-21;
